ISO-10303-21;
HEADER;
/* Generated by software containing ST-Developer
 * from STEP Tools, Inc. (www.steptools.com) 
 */

FILE_DESCRIPTION(
/* description */ ('Bin tilter linkage'),
/* implementation_level */ '2;1');

FILE_NAME(
/* name */ 'M4 short cap screw (5).step',
/* time_stamp */ '2026-10-28T03:26:24-07:00',
/* author */ (''),
/* organization */ (''),
/* preprocessor_version */ 'ST-DEVELOPER v20.2',
/* originating_system */ 'Autodesk Translation Framework v15.17.0.0',
/* authorisation */ '');

FILE_SCHEMA (('AUTOMOTIVE_DESIGN { 1 0 10303 214 3 1 1 }'));
ENDSEC;

DATA;
#10=MECHANICAL_DESIGN_GEOMETRIC_PRESENTATION_REPRESENTATION('',(#900),#23728);
#688=SHAPE_REPRESENTATION_RELATIONSHIP('SRR','None',#24153,#794);
#794=ADVANCED_BREP_SHAPE_REPRESENTATION('',(#1013),#23653);
#900=STYLED_ITEM('',(#24772),#1013);
#1013=MANIFOLD_SOLID_BREP('Body1',#12431);
#1279=FACE_BOUND('',#3166,.T.);
#1640=PLANE('',#14336);
#1641=PLANE('',#14341);
#1642=PLANE('',#14344);
#2196=FACE_OUTER_BOUND('',#3165,.T.);
#2197=FACE_OUTER_BOUND('',#3167,.T.);
#2198=FACE_OUTER_BOUND('',#3168,.T.);
#2199=FACE_OUTER_BOUND('',#3169,.T.);
#2200=FACE_OUTER_BOUND('',#3170,.T.);
#3165=EDGE_LOOP('',(#9589));
#3166=EDGE_LOOP('',(#9590));
#3167=EDGE_LOOP('',(#9591,#9592,#9593,#9594));
#3168=EDGE_LOOP('',(#9595));
#3169=EDGE_LOOP('',(#9596,#9597,#9598,#9599));
#3170=EDGE_LOOP('',(#9600));
#4145=LINE('',#21113,#4820);
#4146=LINE('',#21117,#4821);
#4820=VECTOR('',#17100,0.35);
#4821=VECTOR('',#17105,0.2);
#5511=CIRCLE('',#14337,0.35);
#5512=CIRCLE('',#14338,0.2);
#5513=CIRCLE('',#14340,0.35);
#5514=CIRCLE('',#14343,0.2);
#6361=VERTEX_POINT('',#21106);
#6362=VERTEX_POINT('',#21108);
#6363=VERTEX_POINT('',#21111);
#6364=VERTEX_POINT('',#21116);
#7534=EDGE_CURVE('',#6361,#6361,#5511,.T.);
#7535=EDGE_CURVE('',#6362,#6362,#5512,.T.);
#7536=EDGE_CURVE('',#6363,#6363,#5513,.T.);
#7537=EDGE_CURVE('',#6363,#6361,#4145,.T.);
#7538=EDGE_CURVE('',#6362,#6364,#4146,.T.);
#7539=EDGE_CURVE('',#6364,#6364,#5514,.T.);
#9589=ORIENTED_EDGE('',*,*,#7534,.F.);
#9590=ORIENTED_EDGE('',*,*,#7535,.T.);
#9591=ORIENTED_EDGE('',*,*,#7536,.F.);
#9592=ORIENTED_EDGE('',*,*,#7537,.T.);
#9593=ORIENTED_EDGE('',*,*,#7534,.T.);
#9594=ORIENTED_EDGE('',*,*,#7537,.F.);
#9595=ORIENTED_EDGE('',*,*,#7536,.T.);
#9596=ORIENTED_EDGE('',*,*,#7535,.F.);
#9597=ORIENTED_EDGE('',*,*,#7538,.T.);
#9598=ORIENTED_EDGE('',*,*,#7539,.T.);
#9599=ORIENTED_EDGE('',*,*,#7538,.F.);
#9600=ORIENTED_EDGE('',*,*,#7539,.F.);
#11421=CYLINDRICAL_SURFACE('',#14339,0.35);
#11422=CYLINDRICAL_SURFACE('',#14342,0.2);
#11921=ADVANCED_FACE('',(#2196,#1279),#1640,.F.);
#11922=ADVANCED_FACE('',(#2197),#11421,.T.);
#11923=ADVANCED_FACE('',(#2198),#1641,.T.);
#11924=ADVANCED_FACE('',(#2199),#11422,.T.);
#11925=ADVANCED_FACE('',(#2200),#1642,.F.);
#12431=CLOSED_SHELL('',(#11921,#11922,#11923,#11924,#11925));
#14335=AXIS2_PLACEMENT_3D('',#21104,#17088,#17089);
#14336=AXIS2_PLACEMENT_3D('',#21105,#17090,#17091);
#14337=AXIS2_PLACEMENT_3D('',#21107,#17092,#17093);
#14338=AXIS2_PLACEMENT_3D('',#21109,#17094,#17095);
#14339=AXIS2_PLACEMENT_3D('',#21110,#17096,#17097);
#14340=AXIS2_PLACEMENT_3D('',#21112,#17098,#17099);
#14341=AXIS2_PLACEMENT_3D('',#21114,#17101,#17102);
#14342=AXIS2_PLACEMENT_3D('',#21115,#17103,#17104);
#14343=AXIS2_PLACEMENT_3D('',#21118,#17106,#17107);
#14344=AXIS2_PLACEMENT_3D('',#21119,#17108,#17109);
#17088=DIRECTION('axis',(0.,0.,1.));
#17089=DIRECTION('refdir',(1.,0.,0.));
#17090=DIRECTION('center_axis',(0.,1.,0.));
#17091=DIRECTION('ref_axis',(1.,0.,0.));
#17092=DIRECTION('center_axis',(0.,1.,0.));
#17093=DIRECTION('ref_axis',(1.,0.,0.));
#17094=DIRECTION('center_axis',(0.,1.,0.));
#17095=DIRECTION('ref_axis',(1.,0.,0.));
#17096=DIRECTION('center_axis',(0.,1.,0.));
#17097=DIRECTION('ref_axis',(1.,0.,0.));
#17098=DIRECTION('center_axis',(0.,1.,0.));
#17099=DIRECTION('ref_axis',(1.,0.,0.));
#17100=DIRECTION('',(0.,-1.,0.));
#17101=DIRECTION('center_axis',(0.,1.,0.));
#17102=DIRECTION('ref_axis',(1.,0.,0.));
#17103=DIRECTION('center_axis',(0.,1.,0.));
#17104=DIRECTION('ref_axis',(1.,0.,0.));
#17105=DIRECTION('',(0.,-1.,0.));
#17106=DIRECTION('center_axis',(0.,1.,0.));
#17107=DIRECTION('ref_axis',(1.,0.,0.));
#17108=DIRECTION('center_axis',(0.,1.,0.));
#17109=DIRECTION('ref_axis',(1.,0.,0.));
#21104=CARTESIAN_POINT('',(0.,0.,0.));
#21105=CARTESIAN_POINT('Origin',(-1.30814754519511,0.8,16.3081475451951));
#21106=CARTESIAN_POINT('',(-1.65814754519511,0.8,16.3081475451951));
#21107=CARTESIAN_POINT('Origin',(-1.30814754519511,0.8,16.3081475451951));
#21108=CARTESIAN_POINT('',(-1.50814754519511,0.8,16.3081475451951));
#21109=CARTESIAN_POINT('Origin',(-1.30814754519511,0.8,16.3081475451951));
#21110=CARTESIAN_POINT('Origin',(-1.30814754519511,0.8,16.3081475451951));
#21111=CARTESIAN_POINT('',(-1.65814754519511,1.2,16.3081475451951));
#21112=CARTESIAN_POINT('Origin',(-1.30814754519511,1.2,16.3081475451951));
#21113=CARTESIAN_POINT('',(-1.65814754519511,0.8,16.3081475451951));
#21114=CARTESIAN_POINT('Origin',(-1.30814754519511,1.2,16.3081475451951));
#21115=CARTESIAN_POINT('Origin',(-1.30814754519511,0.1,16.3081475451951));
#21116=CARTESIAN_POINT('',(-1.50814754519511,0.1,16.3081475451951));
#21117=CARTESIAN_POINT('',(-1.50814754519511,0.1,16.3081475451951));
#21118=CARTESIAN_POINT('Origin',(-1.30814754519511,0.1,16.3081475451951));
#21119=CARTESIAN_POINT('Origin',(-1.30814754519511,0.1,16.3081475451951));
#23536=UNCERTAINTY_MEASURE_WITH_UNIT(LENGTH_MEASURE(0.001),#23729,
'DISTANCE_ACCURACY_VALUE',
'Maximum model space distance between geometric entities at asserted c
onnectivities');
#23611=UNCERTAINTY_MEASURE_WITH_UNIT(LENGTH_MEASURE(0.001),#23729,
'DISTANCE_ACCURACY_VALUE',
'Maximum model space distance between geometric entities at asserted c
onnectivities');
#23653=(
GEOMETRIC_REPRESENTATION_CONTEXT(3)
GLOBAL_UNCERTAINTY_ASSIGNED_CONTEXT((#23536))
GLOBAL_UNIT_ASSIGNED_CONTEXT((#23729,#23731,#23732))
REPRESENTATION_CONTEXT('','3D')
);
#23728=(
GEOMETRIC_REPRESENTATION_CONTEXT(3)
GLOBAL_UNCERTAINTY_ASSIGNED_CONTEXT((#23611))
GLOBAL_UNIT_ASSIGNED_CONTEXT((#23729,#23731,#23732))
REPRESENTATION_CONTEXT('','3D')
);
#23729=(
LENGTH_UNIT()
NAMED_UNIT(*)
SI_UNIT(.CENTI.,.METRE.)
);
#23731=(
NAMED_UNIT(*)
PLANE_ANGLE_UNIT()
SI_UNIT($,.RADIAN.)
);
#23732=(
NAMED_UNIT(*)
SI_UNIT($,.STERADIAN.)
SOLID_ANGLE_UNIT()
);
#23774=SHAPE_DEFINITION_REPRESENTATION(#23890,#24153);
#23890=PRODUCT_DEFINITION_SHAPE('',$,#24270);
#24153=SHAPE_REPRESENTATION('',(#14335),#23653);
#24228=PRODUCT_DEFINITION_CONTEXT('part definition',#24578,'design');
#24270=PRODUCT_DEFINITION('M4 short cap screw (5)',
'M4 short cap screw (5)',#24386,#24228);
#24386=PRODUCT_DEFINITION_FORMATION('',$,#24621);
#24578=APPLICATION_CONTEXT(
'Core Data for Automotive Mechanical Design Process');
#24579=PRODUCT_CONTEXT('part definition',#24578,'mechanical');
#24621=PRODUCT('M4 short cap screw (5)','M4 short cap screw (5)',
'M4 short cap screw (5)',(#24579));
#24766=COLOUR_RGB('Black',0.12,0.14,0.17);
#24767=FILL_AREA_STYLE_COLOUR('',#24766);
#24768=FILL_AREA_STYLE('',(#24767));
#24769=SURFACE_STYLE_FILL_AREA(#24768);
#24770=SURFACE_SIDE_STYLE('',(#24769));
#24771=SURFACE_STYLE_USAGE(.BOTH.,#24770);
#24772=PRESENTATION_STYLE_ASSIGNMENT((#24771));
ENDSEC;
END-ISO-10303-21;
